ISO-10303-21;
HEADER;
FILE_DESCRIPTION (('STEP AP214'),
    '1' );
FILE_NAME ('Pusher Guide Rod.step',
    '2026-10-06T10:23:46',
    ( '' ),
    ( '' ),
    'SwSTEP 2.0',
    'SolidWorks 2020',
    '' );
FILE_SCHEMA (( 'AUTOMOTIVE_DESIGN' ));
ENDSEC;

DATA;
#147=CARTESIAN_POINT ( 'NONE',  ( 38.48938833801555148, 40.69123852234599781, 72.28987726642291989 ) ) ;
#402=CARTESIAN_POINT ( 'NONE',  ( 38.31606138205700063, 40.69123852234599781, 71.30501292737000085 ) ) ;
#525=DIRECTION ( 'NONE',  ( 0.000000000000000000, 1.000000000000000000, -2.999999999999999839E-15 ) ) ;
#558=CARTESIAN_POINT ( 'NONE',  ( 38.31606138205700063, 37.69123852234599781, 71.30501292737001506 ) ) ;
#578=CARTESIAN_POINT ( 'NONE',  ( 38.31606138205700063, 37.69123852234599781, 71.30501292737001506 ) ) ;
#580=ORIENTED_EDGE ( 'NONE', *, *, #7197, .F. ) ;
#693=( NAMED_UNIT ( * ) PLANE_ANGLE_UNIT ( ) SI_UNIT ( $, .RADIAN. ) );
#739=APPLICATION_CONTEXT ( 'automotive_design' ) ;
#852=AXIS2_PLACEMENT_3D ( 'NONE', #7427, #17477, #15521 ) ;
#918=CIRCLE ( 'NONE', #18590, 0.9999999999999937828 ) ;
#943=AXIS2_PLACEMENT_3D ( 'NONE', #9955, #8026, #8404 ) ;
#1013=CARTESIAN_POINT ( 'NONE',  ( 38.14273442609844977, 37.69123852234599781, 70.32014858831708182 ) ) ;
#1116=CLOSED_SHELL ( 'NONE', ( #23082, #8314, #18083, #5885, #3587, #15410, #23487, #24644, #1224, #14054 ) ) ;
#1224=ADVANCED_FACE ( 'NONE', ( #14501 ), #8936, .T. ) ;
#1226=EDGE_CURVE ( 'NONE', #15804, #2469, #13867, .T. ) ;
#1234=FILL_AREA_STYLE_COLOUR ( '', #7978 ) ;
#1250=CARTESIAN_POINT ( 'NONE',  ( 38.31606138205700063, 37.69123852234599781, 71.30501292737001506 ) ) ;
#1387=EDGE_CURVE ( 'NONE', #21411, #6994, #5221, .T. ) ;
#1607=DIRECTION ( 'NONE',  ( 2.122643018205885151E-17, -1.000000000000000000, 3.120611096041553009E-15 ) ) ;
#1731=PLANE ( 'NONE',  #18014 ) ;
#1868=ORIENTED_EDGE ( 'NONE', *, *, #21287, .F. ) ;
#1900=EDGE_LOOP ( 'NONE', ( #6401, #1993 ) ) ;
#1943=LINE ( 'NONE', #147, #23590 ) ;
#1993=ORIENTED_EDGE ( 'NONE', *, *, #21629, .F. ) ;
#2000=AXIS2_PLACEMENT_3D ( 'NONE', #9286, #12766, #22537 ) ;
#2009=EDGE_CURVE ( 'NONE', #18901, #16151, #5224, .T. ) ;
#2106=COLOUR_RGB ( '', 0.40784314, 0.44705882, 0.49803922) ;
#2413=CARTESIAN_POINT ( 'NONE',  ( 38.53272007700518742, 38.19123852234600491, 72.53609335118615320 ) ) ;
#2465=DIRECTION ( 'NONE',  ( -0.1733269559585509378, 0.000000000000000000, -0.9848643390529188135 ) ) ;
#2469=VERTEX_POINT ( 'NONE', #20147 ) ;
#2520=EDGE_CURVE ( 'NONE', #16389, #15899, #14302, .T. ) ;
#2729=AXIS2_PLACEMENT_3D ( 'NONE', #578, #14375, #12463 ) ;
#2856=CARTESIAN_POINT ( 'NONE',  ( 38.31606138205700063, 38.69123852234599781, 71.30501292737000085 ) ) ;
#3011=ORIENTED_EDGE ( 'NONE', *, *, #12594, .T. ) ;
#3012=( NAMED_UNIT ( * ) SI_UNIT ( $, .STERADIAN. ) SOLID_ANGLE_UNIT ( ) );
#3025=ORIENTED_EDGE ( 'NONE', *, *, #3131, .T. ) ;
#3131=EDGE_CURVE ( 'NONE', #15899, #16389, #25430, .T. ) ;
#3340=DIRECTION ( 'NONE',  ( -2.122643018205887308E-17, 1.000000000000000000, -3.120611096041553009E-15 ) ) ;
#3455=EDGE_LOOP ( 'NONE', ( #580, #12966, #3011, #22594 ) ) ;
#3543=( LENGTH_UNIT ( ) NAMED_UNIT ( * ) SI_UNIT ( .MILLI., .METRE. ) );
#3587=ADVANCED_FACE ( 'NONE', ( #8496, #22265 ), #10685, .T. ) ;
#3599=ORIENTED_EDGE ( 'NONE', *, *, #21665, .T. ) ;
#3671=CYLINDRICAL_SURFACE ( 'NONE', #852, 0.9999999999999937828 ) ;
#3686=CIRCLE ( 'NONE', #21376, 1.249999999999995115 ) ;
#3858=DIRECTION ( 'NONE',  ( -0.1733269559585509378, 0.000000000000000000, -0.9848643390529188135 ) ) ;
#4206=VECTOR ( 'NONE', #14399, 1000.000000000000000 ) ;
#4370=APPLICATION_CONTEXT ( 'automotive_design' ) ;
#4653=AXIS2_PLACEMENT_3D ( 'NONE', #402, #14081, #2465 ) ;
#4702=ORIENTED_EDGE ( 'NONE', *, *, #2520, .T. ) ;
#4860=CARTESIAN_POINT ( 'NONE',  ( 38.48938833801555148, 40.69123852234599781, 72.28987726642291989 ) ) ;
#4961=SURFACE_STYLE_FILL_AREA ( #6513 ) ;
#4988=EDGE_LOOP ( 'NONE', ( #19095, #11900 ) ) ;
#5133=AXIS2_PLACEMENT_3D ( 'NONE', #7789, #17837, #11790 ) ;
#5221=LINE ( 'NONE', #13085, #15128 ) ;
#5224=CIRCLE ( 'NONE', #14282, 1.249999999999995115 ) ;
#5237=VERTEX_POINT ( 'NONE', #13924 ) ;
#5466=ORIENTED_EDGE ( 'NONE', *, *, #21629, .T. ) ;
#5491=FILL_AREA_STYLE ('',( #1234 ) ) ;
#5495=FACE_OUTER_BOUND ( 'NONE', #7713, .T. ) ;
#5547=ORIENTED_EDGE ( 'NONE', *, *, #22637, .T. ) ;
#5578=AXIS2_PLACEMENT_3D ( 'NONE', #24330, #8264, #6334 ) ;
#5600=EDGE_LOOP ( 'NONE', ( #6712, #11975 ) ) ;
#5885=ADVANCED_FACE ( 'NONE', ( #19239 ), #13768, .T. ) ;
#5907=PRODUCT_DEFINITION_CONTEXT ( 'detailed design', #739, 'design' ) ;
#6027=DIRECTION ( 'NONE',  ( 0.000000000000000000, 1.000000000000000000, -2.999999999999999839E-15 ) ) ;
#6130=ADVANCED_BREP_SHAPE_REPRESENTATION ( '', ( #25224, #2000 ), #15364 ) ;
#6155=AXIS2_PLACEMENT_3D ( 'NONE', #9741, #25034, #17592 ) ;
#6192=UNCERTAINTY_MEASURE_WITH_UNIT (LENGTH_MEASURE( 1.000000000000000082E-05 ), #10911, 'distance_accuracy_value', 'NONE');
#6334=DIRECTION ( 'NONE',  ( -0.1733269559585509378, 0.000000000000000000, -0.9848643390529188135 ) ) ;
#6401=ORIENTED_EDGE ( 'NONE', *, *, #9133, .F. ) ;
#6513=FILL_AREA_STYLE ('',( #9096 ) ) ;
#6667=DIRECTION ( 'NONE',  ( -0.1733269559585509378, 0.000000000000000000, -0.9848643390529188135 ) ) ;
#6712=ORIENTED_EDGE ( 'NONE', *, *, #16483, .T. ) ;
#6849=ORIENTED_EDGE ( 'NONE', *, *, #21665, .F. ) ;
#6888=( LENGTH_UNIT ( ) NAMED_UNIT ( * ) SI_UNIT ( .MILLI., .METRE. ) );
#6994=VERTEX_POINT ( 'NONE', #1013 ) ;
#7037=( NAMED_UNIT ( * ) PLANE_ANGLE_UNIT ( ) SI_UNIT ( $, .RADIAN. ) );
#7079=CARTESIAN_POINT ( 'NONE',  ( 38.48938833801555148, 37.69123852234600491, 72.28987726642293410 ) ) ;
#7091=CARTESIAN_POINT ( 'NONE',  ( 38.31606138205700063, 38.69123852234599781, 71.30501292737000085 ) ) ;
#7114=CARTESIAN_POINT ( 'NONE',  ( 38.53272007700518742, 37.69123852234600491, 72.53609335118615320 ) ) ;
#7197=EDGE_CURVE ( 'NONE', #15804, #18901, #20281, .T. ) ;
#7427=CARTESIAN_POINT ( 'NONE',  ( 38.31606138205700063, 40.69123852234599781, 71.30501292737000085 ) ) ;
#7512=EDGE_CURVE ( 'NONE', #16332, #6994, #918, .T. ) ;
#7635=DIRECTION ( 'NONE',  ( 0.000000000000000000, 1.000000000000000000, -2.999999999999999839E-15 ) ) ;
#7662=PRODUCT ( 'Pusher Guide Rod', 'Pusher Guide Rod', '', ( #13059 ) ) ;
#7713=EDGE_LOOP ( 'NONE', ( #3025, #11136, #23372, #25200 ) ) ;
#7786=CYLINDRICAL_SURFACE ( 'NONE', #24792, 0.9999999999999937828 ) ;
#7789=CARTESIAN_POINT ( 'NONE',  ( 38.31606138205700063, 40.69123852234599781, 71.30501292737000085 ) ) ;
#7944=DIRECTION ( 'NONE',  ( -0.1733269559585470521, -3.077057697073492856E-15, -0.9848643390529193686 ) ) ;
#7978=COLOUR_RGB ( '', 0.40784314, 0.44705882, 0.49803922) ;
#8026=DIRECTION ( 'NONE',  ( 0.9848643390529194797, -5.199808678756412277E-16, -0.1733269559585470798 ) ) ;
#8037=CYLINDRICAL_SURFACE ( 'NONE', #4653, 0.9999999999999937828 ) ;
#8129=CARTESIAN_POINT ( 'NONE',  ( 38.09940268710882094, 38.69123852234599781, 70.07393250355386272 ) ) ;
#8204=AXIS2_PLACEMENT_3D ( 'NONE', #18682, #3340, #11217 ) ;
#8264=DIRECTION ( 'NONE',  ( 0.000000000000000000, 1.000000000000000000, -2.999999999999999839E-15 ) ) ;
#8314=ADVANCED_FACE ( 'NONE', ( #10952 ), #20616, .T. ) ;
#8404=DIRECTION ( 'NONE',  ( 0.000000000000000000, -1.000000000000000000, 0.000000000000000000 ) ) ;
#8496=FACE_BOUND ( 'NONE', #4988, .T. ) ;
#8719=MECHANICAL_DESIGN_GEOMETRIC_PRESENTATION_REPRESENTATION('',(#16505),#12306);
#8936=TOROIDAL_SURFACE ( 'NONE', #23312, 1.250000000000000000, 0.5000000000000000000 ) ;
#9096=FILL_AREA_STYLE_COLOUR ( '', #2106 ) ;
#9133=EDGE_CURVE ( 'NONE', #21411, #5237, #9706, .T. ) ;
#9286=CARTESIAN_POINT ( 'NONE',  ( 0.000000000000000000, 0.000000000000000000, 0.000000000000000000 ) ) ;
#9305=FACE_OUTER_BOUND ( 'NONE', #5600, .T. ) ;
#9345=DIRECTION ( 'NONE',  ( -0.1733269559585479680, -3.077057697073492856E-15, -0.9848643390529192576 ) ) ;
#9480=ORIENTED_EDGE ( 'NONE', *, *, #11787, .T. ) ;
#9706=CIRCLE ( 'NONE', #5578, 0.9999999999999937828 ) ;
#9741=CARTESIAN_POINT ( 'NONE',  ( 38.14273442609844977, -33.30876147765400219, 70.32014858831730919 ) ) ;
#9915=DIRECTION ( 'NONE',  ( 0.1733269559585485786, 0.000000000000000000, 0.9848643390529193686 ) ) ;
#9955=CARTESIAN_POINT ( 'NONE',  ( 38.09940268710882094, 38.19123852234599781, 70.07393250355386272 ) ) ;
#10107=PRODUCT_DEFINITION ( 'UNKNOWN', '', #18289, #5907 ) ;
#10119=DIRECTION ( 'NONE',  ( 0.000000000000000000, 1.000000000000000000, -2.999999999999999839E-15 ) ) ;
#10122=EDGE_LOOP ( 'NONE', ( #10694, #5466, #17396, #16671 ) ) ;
#10167=CIRCLE ( 'NONE', #23723, 0.9999999999999937828 ) ;
#10251=AXIS2_PLACEMENT_3D ( 'NONE', #7091, #13152, #3858 ) ;
#10266=SHAPE_REPRESENTATION ( 'Pusher Guide Rod', ( #2000 ), #15364 ) ;
#10275=CIRCLE ( 'NONE', #13161, 1.249999999999995115 ) ;
#10293=AXIS2_PLACEMENT_3D ( 'NONE', #11744, #15582, #21516 ) ;
#10685=PLANE ( 'NONE',  #11914 ) ;
#10694=ORIENTED_EDGE ( 'NONE', *, *, #11787, .F. ) ;
#10911=( LENGTH_UNIT ( ) NAMED_UNIT ( * ) SI_UNIT ( .MILLI., .METRE. ) );
#10952=FACE_OUTER_BOUND ( 'NONE', #10122, .T. ) ;
#11035=PRESENTATION_STYLE_ASSIGNMENT (( #15273 ) ) ;
#11136=ORIENTED_EDGE ( 'NONE', *, *, #12599, .T. ) ;
#11213=DIRECTION ( 'NONE',  ( -0.1733269559585509378, 0.000000000000000000, -0.9848643390529188135 ) ) ;
#11217=DIRECTION ( 'NONE',  ( -0.1733269559585509378, 0.000000000000000000, -0.9848643390529188135 ) ) ;
#11258=DIRECTION ( 'NONE',  ( 0.000000000000000000, 1.000000000000000000, -2.999999999999999839E-15 ) ) ;
#11268=MECHANICAL_DESIGN_GEOMETRIC_PRESENTATION_REPRESENTATION('',(#22363),#25222);
#11532=ORIENTED_EDGE ( 'NONE', *, *, #9133, .T. ) ;
#11581=PRODUCT_DEFINITION_SHAPE ( 'NONE', 'NONE',  #10107 ) ;
#11593=CARTESIAN_POINT ( 'NONE',  ( 38.31606138205700063, 40.69123852234599781, 71.30501292737000085 ) ) ;
#11744=CARTESIAN_POINT ( 'NONE',  ( 38.31606138205700063, 40.69123852234599781, 71.30501292737000085 ) ) ;
#11775=CARTESIAN_POINT ( 'NONE',  ( 38.31606138205700063, 37.69123852234599781, 71.30501292737001506 ) ) ;
#11787=EDGE_CURVE ( 'NONE', #5237, #16332, #24526, .T. ) ;
#11790=DIRECTION ( 'NONE',  ( -0.1733269559585509378, 0.000000000000000000, -0.9848643390529188135 ) ) ;
#11900=ORIENTED_EDGE ( 'NONE', *, *, #2520, .F. ) ;
#11914=AXIS2_PLACEMENT_3D ( 'NONE', #18657, #16330, #24437 ) ;
#11971=DIRECTION ( 'NONE',  ( -0.1733269559585477460, -5.551115123125804790E-15, -0.9848643390529193686 ) ) ;
#11975=ORIENTED_EDGE ( 'NONE', *, *, #16964, .T. ) ;
#12098=ORIENTED_EDGE ( 'NONE', *, *, #16964, .F. ) ;
#12306=( GEOMETRIC_REPRESENTATION_CONTEXT ( 3 ) GLOBAL_UNCERTAINTY_ASSIGNED_CONTEXT ( ( #19780 ) ) GLOBAL_UNIT_ASSIGNED_CONTEXT ( ( #6888, #693, #3012 ) ) REPRESENTATION_CONTEXT ( 'NONE', 'WORKASPACE' ) );
#12463=DIRECTION ( 'NONE',  ( -0.1733269559585477460, -5.551115123125804790E-15, -0.9848643390529193686 ) ) ;
#12594=EDGE_CURVE ( 'NONE', #2469, #16151, #17016, .T. ) ;
#12599=EDGE_CURVE ( 'NONE', #16389, #14611, #1943, .T. ) ;
#12659=AXIS2_PLACEMENT_3D ( 'NONE', #2856, #11258, #24487 ) ;
#12741=DIRECTION ( 'NONE',  ( 0.000000000000000000, 1.000000000000000000, -2.999999999999999839E-15 ) ) ;
#12766=DIRECTION ( 'NONE',  ( 0.000000000000000000, 0.000000000000000000, 1.000000000000000000 ) ) ;
#12830=PRESENTATION_STYLE_ASSIGNMENT (( #24515 ) ) ;
#12879=AXIS2_PLACEMENT_3D ( 'NONE', #2413, #14275, #9915 ) ;
#12930=CIRCLE ( 'NONE', #21565, 0.9999999999999937828 ) ;
#12966=ORIENTED_EDGE ( 'NONE', *, *, #1226, .T. ) ;
#12978=( NAMED_UNIT ( * ) SI_UNIT ( $, .STERADIAN. ) SOLID_ANGLE_UNIT ( ) );
#13059=PRODUCT_CONTEXT ( 'NONE', #4370, 'mechanical' ) ;
#13085=CARTESIAN_POINT ( 'NONE',  ( 38.14273442609844977, 40.69123852234599781, 70.32014858831708182 ) ) ;
#13101=( NAMED_UNIT ( * ) SI_UNIT ( $, .STERADIAN. ) SOLID_ANGLE_UNIT ( ) );
#13152=DIRECTION ( 'NONE',  ( 0.000000000000000000, 1.000000000000000000, -2.999999999999999839E-15 ) ) ;
#13161=AXIS2_PLACEMENT_3D ( 'NONE', #13884, #6027, #11971 ) ;
#13336=DIRECTION ( 'NONE',  ( -0.1733269559585509378, 0.000000000000000000, -0.9848643390529188135 ) ) ;
#13459=ORIENTED_EDGE ( 'NONE', *, *, #21287, .T. ) ;
#13683=CARTESIAN_POINT ( 'NONE',  ( 38.31606138205700063, 38.69123852234599781, 71.30501292737000085 ) ) ;
#13694=CARTESIAN_POINT ( 'NONE',  ( 38.31606138205700063, -33.30876147765400219, 71.30501292737024244 ) ) ;
#13768=TOROIDAL_SURFACE ( 'NONE', #16618, 1.250000000000000000, 0.5000000000000000000 ) ;
#13815=DIRECTION ( 'NONE',  ( -0.1733269559585509378, 0.000000000000000000, -0.9848643390529188135 ) ) ;
#13867=CIRCLE ( 'NONE', #2729, 1.249999999999995115 ) ;
#13884=CARTESIAN_POINT ( 'NONE',  ( 38.31606138205700063, 38.69123852234599781, 71.30501292737000085 ) ) ;
#13924=CARTESIAN_POINT ( 'NONE',  ( 38.48938833801555148, -33.30876147765400219, 72.28987726642316147 ) ) ;
#14054=ADVANCED_FACE ( 'NONE', ( #20001 ), #8037, .T. ) ;
#14081=DIRECTION ( 'NONE',  ( -2.122643018205887308E-17, 1.000000000000000000, -3.120611096041553009E-15 ) ) ;
#14267=ORIENTED_EDGE ( 'NONE', *, *, #7197, .T. ) ;
#14275=DIRECTION ( 'NONE',  ( -0.9848643390529194797, 5.199808678756408333E-16, 0.1733269559585469688 ) ) ;
#14282=AXIS2_PLACEMENT_3D ( 'NONE', #13683, #7635, #21542 ) ;
#14302=CIRCLE ( 'NONE', #12659, 0.9999999999999937828 ) ;
#14375=DIRECTION ( 'NONE',  ( 0.000000000000000000, 1.000000000000000000, -2.999999999999999839E-15 ) ) ;
#14399=DIRECTION ( 'NONE',  ( -2.122643018205887308E-17, 1.000000000000000000, -3.120611096041553009E-15 ) ) ;
#14501=FACE_OUTER_BOUND ( 'NONE', #23405, .T. ) ;
#14611=VERTEX_POINT ( 'NONE', #4860 ) ;
#14747=EDGE_CURVE ( 'NONE', #15899, #15633, #16317, .T. ) ;
#14775=ORIENTED_EDGE ( 'NONE', *, *, #1387, .F. ) ;
#15088=CIRCLE ( 'NONE', #17584, 0.9999999999999937828 ) ;
#15128=VECTOR ( 'NONE', #20937, 1000.000000000000000 ) ;
#15273=SURFACE_STYLE_USAGE ( .BOTH. , #18633 ) ;
#15364=( GEOMETRIC_REPRESENTATION_CONTEXT ( 3 ) GLOBAL_UNCERTAINTY_ASSIGNED_CONTEXT ( ( #23943 ) ) GLOBAL_UNIT_ASSIGNED_CONTEXT ( ( #3543, #7037, #12978 ) ) REPRESENTATION_CONTEXT ( 'NONE', 'WORKASPACE' ) );
#15410=ADVANCED_FACE ( 'NONE', ( #19618 ), #7786, .T. ) ;
#15521=DIRECTION ( 'NONE',  ( -0.1733269559585509378, 0.000000000000000000, -0.9848643390529188135 ) ) ;
#15582=DIRECTION ( 'NONE',  ( -2.122643018205885151E-17, 1.000000000000000000, -3.120611096041553009E-15 ) ) ;
#15633=VERTEX_POINT ( 'NONE', #22060 ) ;
#15646=ORIENTED_EDGE ( 'NONE', *, *, #2009, .T. ) ;
#15804=VERTEX_POINT ( 'NONE', #7114 ) ;
#15899=VERTEX_POINT ( 'NONE', #24867 ) ;
#16032=EDGE_LOOP ( 'NONE', ( #3599, #23662 ) ) ;
#16151=VERTEX_POINT ( 'NONE', #8129 ) ;
#16242=DIRECTION ( 'NONE',  ( -2.122643018205887308E-17, 1.000000000000000000, -3.120611096041553009E-15 ) ) ;
#16294=CARTESIAN_POINT ( 'NONE',  ( 38.31606138205700063, 38.19123852234599781, 71.30501292737001506 ) ) ;
#16317=LINE ( 'NONE', #20200, #4206 ) ;
#16330=DIRECTION ( 'NONE',  ( -2.122643018205885151E-17, 1.000000000000000000, -3.120611096041553009E-15 ) ) ;
#16332=VERTEX_POINT ( 'NONE', #7079 ) ;
#16389=VERTEX_POINT ( 'NONE', #16739 ) ;
#16483=EDGE_CURVE ( 'NONE', #15633, #14611, #12930, .T. ) ;
#16505=STYLED_ITEM ( 'NONE', ( #12830 ), #25224 ) ;
#16618=AXIS2_PLACEMENT_3D ( 'NONE', #16679, #22602, #9345 ) ;
#16671=ORIENTED_EDGE ( 'NONE', *, *, #7512, .F. ) ;
#16679=CARTESIAN_POINT ( 'NONE',  ( 38.31606138205700063, 38.19123852234599781, 71.30501292737001506 ) ) ;
#16739=CARTESIAN_POINT ( 'NONE',  ( 38.48938833801555148, 38.69123852234600491, 72.28987726642293410 ) ) ;
#16822=DIRECTION ( 'NONE',  ( -2.122643018205887308E-17, 1.000000000000000000, -3.120611096041553009E-15 ) ) ;
#16964=EDGE_CURVE ( 'NONE', #14611, #15633, #21583, .T. ) ;
#17016=CIRCLE ( 'NONE', #943, 0.5000000000000004441 ) ;
#17147=PLANE ( 'NONE',  #10293 ) ;
#17213=PLANE ( 'NONE',  #6155 ) ;
#17215=SHAPE_REPRESENTATION_RELATIONSHIP ( 'NONE' , 'NONE' ,  #10266, #6130 ) ;
#17321=CARTESIAN_POINT ( 'NONE',  ( 38.31606138205700063, 40.69123852234599781, 71.30501292737000085 ) ) ;
#17396=ORIENTED_EDGE ( 'NONE', *, *, #1387, .T. ) ;
#17477=DIRECTION ( 'NONE',  ( -2.122643018205887308E-17, 1.000000000000000000, -3.120611096041553009E-15 ) ) ;
#17584=AXIS2_PLACEMENT_3D ( 'NONE', #11775, #525, #21928 ) ;
#17592=DIRECTION ( 'NONE',  ( -0.1733269559585470521, -3.077057697073492856E-15, -0.9848643390529193686 ) ) ;
#17729=CARTESIAN_POINT ( 'NONE',  ( 38.09940268710882094, 37.69123852234599781, 70.07393250355386272 ) ) ;
#17837=DIRECTION ( 'NONE',  ( -2.122643018205887308E-17, 1.000000000000000000, -3.120611096041553009E-15 ) ) ;
#18000=DIRECTION ( 'NONE',  ( -0.1733269559585479680, -3.077057697073492856E-15, -0.9848643390529192576 ) ) ;
#18014=AXIS2_PLACEMENT_3D ( 'NONE', #17729, #1607, #7944 ) ;
#18083=ADVANCED_FACE ( 'NONE', ( #25041, #25169 ), #1731, .T. ) ;
#18251=DIRECTION ( 'NONE',  ( -2.122643018205887308E-17, 1.000000000000000000, -3.120611096041553009E-15 ) ) ;
#18289=PRODUCT_DEFINITION_FORMATION_WITH_SPECIFIED_SOURCE ( 'ANY', '', #7662, .NOT_KNOWN. ) ;
#18590=AXIS2_PLACEMENT_3D ( 'NONE', #1250, #12741, #6667 ) ;
#18633=SURFACE_SIDE_STYLE ('',( #18762 ) ) ;
#18657=CARTESIAN_POINT ( 'NONE',  ( 38.14273442609844977, 38.69123852234599781, 70.32014858831708182 ) ) ;
#18682=CARTESIAN_POINT ( 'NONE',  ( 38.31606138205700063, 40.69123852234599781, 71.30501292737000085 ) ) ;
#18703=EDGE_LOOP ( 'NONE', ( #1868, #19531 ) ) ;
#18762=SURFACE_STYLE_FILL_AREA ( #5491 ) ;
#18901=VERTEX_POINT ( 'NONE', #22488 ) ;
#19053=ORIENTED_EDGE ( 'NONE', *, *, #12599, .F. ) ;
#19095=ORIENTED_EDGE ( 'NONE', *, *, #3131, .F. ) ;
#19239=FACE_OUTER_BOUND ( 'NONE', #3455, .T. ) ;
#19531=ORIENTED_EDGE ( 'NONE', *, *, #1226, .F. ) ;
#19563=DIRECTION ( 'NONE',  ( -2.122643018205887308E-17, 1.000000000000000000, -3.120611096041553009E-15 ) ) ;
#19618=FACE_OUTER_BOUND ( 'NONE', #23768, .T. ) ;
#19780=UNCERTAINTY_MEASURE_WITH_UNIT (LENGTH_MEASURE( 1.000000000000000082E-05 ), #6888, 'distance_accuracy_value', 'NONE');
#19872=DIRECTION ( 'NONE',  ( 0.000000000000000000, 1.000000000000000000, -2.999999999999999839E-15 ) ) ;
#20001=FACE_OUTER_BOUND ( 'NONE', #25433, .T. ) ;
#20147=CARTESIAN_POINT ( 'NONE',  ( 38.09940268710882094, 37.69123852234599781, 70.07393250355386272 ) ) ;
#20200=CARTESIAN_POINT ( 'NONE',  ( 38.14273442609844977, 40.69123852234599781, 70.32014858831708182 ) ) ;
#20281=CIRCLE ( 'NONE', #12879, 0.5000000000000036637 ) ;
#20418=SURFACE_SIDE_STYLE ('',( #4961 ) ) ;
#20616=CYLINDRICAL_SURFACE ( 'NONE', #8204, 0.9999999999999937828 ) ;
#20666=EDGE_LOOP ( 'NONE', ( #5547, #15646 ) ) ;
#20692=CARTESIAN_POINT ( 'NONE',  ( 38.48938833801555148, 40.69123852234599781, 72.28987726642291989 ) ) ;
#20699=( NAMED_UNIT ( * ) PLANE_ANGLE_UNIT ( ) SI_UNIT ( $, .RADIAN. ) );
#20937=DIRECTION ( 'NONE',  ( -2.122643018205887308E-17, 1.000000000000000000, -3.120611096041553009E-15 ) ) ;
#21201=FACE_OUTER_BOUND ( 'NONE', #1900, .T. ) ;
#21287=EDGE_CURVE ( 'NONE', #2469, #15804, #3686, .T. ) ;
#21376=AXIS2_PLACEMENT_3D ( 'NONE', #558, #10119, #22079 ) ;
#21411=VERTEX_POINT ( 'NONE', #23757 ) ;
#21516=DIRECTION ( 'NONE',  ( -0.1733269559585470521, -3.077057697073492856E-15, -0.9848643390529193686 ) ) ;
#21542=DIRECTION ( 'NONE',  ( -0.1733269559585477460, -5.551115123125804790E-15, -0.9848643390529193686 ) ) ;
#21565=AXIS2_PLACEMENT_3D ( 'NONE', #11593, #19563, #11213 ) ;
#21566=DIRECTION ( 'NONE',  ( -2.122643018205887308E-17, 1.000000000000000000, -3.120611096041553009E-15 ) ) ;
#21583=CIRCLE ( 'NONE', #5133, 0.9999999999999937828 ) ;
#21629=EDGE_CURVE ( 'NONE', #5237, #21411, #10167, .T. ) ;
#21665=EDGE_CURVE ( 'NONE', #6994, #16332, #15088, .T. ) ;
#21928=DIRECTION ( 'NONE',  ( -0.1733269559585509378, 0.000000000000000000, -0.9848643390529188135 ) ) ;
#22060=CARTESIAN_POINT ( 'NONE',  ( 38.14273442609844977, 40.69123852234599781, 70.32014858831708182 ) ) ;
#22079=DIRECTION ( 'NONE',  ( -0.1733269559585477460, -5.551115123125804790E-15, -0.9848643390529193686 ) ) ;
#22265=FACE_OUTER_BOUND ( 'NONE', #20666, .T. ) ;
#22363=STYLED_ITEM ( 'NONE', ( #11035 ), #6130 ) ;
#22488=CARTESIAN_POINT ( 'NONE',  ( 38.53272007700518742, 38.69123852234600491, 72.53609335118615320 ) ) ;
#22537=DIRECTION ( 'NONE',  ( 1.000000000000000000, 0.000000000000000000, 0.000000000000000000 ) ) ;
#22594=ORIENTED_EDGE ( 'NONE', *, *, #2009, .F. ) ;
#22602=DIRECTION ( 'NONE',  ( -2.122643018205887308E-17, 1.000000000000000000, -3.120611096041553009E-15 ) ) ;
#22637=EDGE_CURVE ( 'NONE', #16151, #18901, #10275, .T. ) ;
#22972=ORIENTED_EDGE ( 'NONE', *, *, #14747, .T. ) ;
#23080=SHAPE_DEFINITION_REPRESENTATION ( #11581, #10266 ) ;
#23082=ADVANCED_FACE ( 'NONE', ( #21201 ), #17213, .T. ) ;
#23144=VECTOR ( 'NONE', #16822, 1000.000000000000000 ) ;
#23312=AXIS2_PLACEMENT_3D ( 'NONE', #16294, #18251, #18000 ) ;
#23372=ORIENTED_EDGE ( 'NONE', *, *, #16483, .F. ) ;
#23405=EDGE_LOOP ( 'NONE', ( #13459, #14267, #24943, #25410 ) ) ;
#23487=ADVANCED_FACE ( 'NONE', ( #9305 ), #17147, .T. ) ;
#23590=VECTOR ( 'NONE', #16242, 1000.000000000000000 ) ;
#23662=ORIENTED_EDGE ( 'NONE', *, *, #7512, .T. ) ;
#23723=AXIS2_PLACEMENT_3D ( 'NONE', #13694, #19872, #13815 ) ;
#23757=CARTESIAN_POINT ( 'NONE',  ( 38.14273442609844977, -33.30876147765400219, 70.32014858831730919 ) ) ;
#23768=EDGE_LOOP ( 'NONE', ( #19053, #4702, #22972, #12098 ) ) ;
#23943=UNCERTAINTY_MEASURE_WITH_UNIT (LENGTH_MEASURE( 1.000000000000000082E-05 ), #3543, 'distance_accuracy_value', 'NONE');
#24330=CARTESIAN_POINT ( 'NONE',  ( 38.31606138205700063, -33.30876147765400219, 71.30501292737024244 ) ) ;
#24437=DIRECTION ( 'NONE',  ( -0.1733269559585470521, -3.077057697073492856E-15, -0.9848643390529193686 ) ) ;
#24487=DIRECTION ( 'NONE',  ( -0.1733269559585509378, 0.000000000000000000, -0.9848643390529188135 ) ) ;
#24515=SURFACE_STYLE_USAGE ( .BOTH. , #20418 ) ;
#24526=LINE ( 'NONE', #20692, #23144 ) ;
#24644=ADVANCED_FACE ( 'NONE', ( #5495 ), #3671, .T. ) ;
#24792=AXIS2_PLACEMENT_3D ( 'NONE', #17321, #21566, #13336 ) ;
#24867=CARTESIAN_POINT ( 'NONE',  ( 38.14273442609844977, 38.69123852234599781, 70.32014858831708182 ) ) ;
#24943=ORIENTED_EDGE ( 'NONE', *, *, #22637, .F. ) ;
#25034=DIRECTION ( 'NONE',  ( 2.122643018205885151E-17, -1.000000000000000000, 3.120611096041553009E-15 ) ) ;
#25041=FACE_BOUND ( 'NONE', #16032, .T. ) ;
#25169=FACE_OUTER_BOUND ( 'NONE', #18703, .T. ) ;
#25200=ORIENTED_EDGE ( 'NONE', *, *, #14747, .F. ) ;
#25222=( GEOMETRIC_REPRESENTATION_CONTEXT ( 3 ) GLOBAL_UNCERTAINTY_ASSIGNED_CONTEXT ( ( #6192 ) ) GLOBAL_UNIT_ASSIGNED_CONTEXT ( ( #10911, #20699, #13101 ) ) REPRESENTATION_CONTEXT ( 'NONE', 'WORKASPACE' ) );
#25224=MANIFOLD_SOLID_BREP ( 'NONE', #1116 ) ;
#25410=ORIENTED_EDGE ( 'NONE', *, *, #12594, .F. ) ;
#25430=CIRCLE ( 'NONE', #10251, 0.9999999999999937828 ) ;
#25433=EDGE_LOOP ( 'NONE', ( #11532, #9480, #6849, #14775 ) ) ;
ENDSEC;
END-ISO-10303-21;
